ISO-10303-21;
HEADER;
FILE_DESCRIPTION (('STEP AP214'),
    '1' );
FILE_NAME ('socket head cap screw_iso_ISO 4762 M5 x 20 - 20N.step',
    '2026-10-24T11:01:53',
    ( '' ),
    ( '' ),
    'SwSTEP 2.0',
    'SolidWorks 2026',
    '' );
FILE_SCHEMA (( 'AUTOMOTIVE_DESIGN' ));
ENDSEC;

DATA;
#6=ORIENTED_EDGE ( 'NONE', *, *, #8549, .T. ) ;
#27=AXIS2_PLACEMENT_3D ( 'NONE', #2373, #401, #2287 ) ;
#43=VECTOR ( 'NONE', #8305, 1000.000000000000000 ) ;
#82=FACE_OUTER_BOUND ( 'NONE', #3870, .T. ) ;
#83=DIRECTION ( 'NONE',  ( 0.000000000000000000, 1.000000000000000000, -1.224646799147353207E-16 ) ) ;
#109=CARTESIAN_POINT ( 'NONE',  ( 2.500000000000000000, -2.357898499370432610, 3.252606517456513302E-15 ) ) ;
#121=EDGE_CURVE ( 'NONE', #848, #6261, #4955, .T. ) ;
#133=VERTEX_POINT ( 'NONE', #5381 ) ;
#134=ORIENTED_EDGE ( 'NONE', *, *, #577, .F. ) ;
#136=CARTESIAN_POINT ( 'NONE',  ( 5.200000000000002842, 0.000000000000000000, 0.000000000000000000 ) ) ;
#146=ORIENTED_EDGE ( 'NONE', *, *, #2955, .F. ) ;
#163=AXIS2_PLACEMENT_3D ( 'NONE', #2738, #6866, #8185 ) ;
#180=FACE_OUTER_BOUND ( 'NONE', #6238, .T. ) ;
#188=AXIS2_PLACEMENT_3D ( 'NONE', #1470, #2312, #5600 ) ;
#195=ORIENTED_EDGE ( 'NONE', *, *, #2103, .T. ) ;
#197=ORIENTED_EDGE ( 'NONE', *, *, #8549, .F. ) ;
#199=LINE ( 'NONE', #109, #2686 ) ;
#205=EDGE_LOOP ( 'NONE', ( #3377, #2708, #3333, #2786 ) ) ;
#212=DIRECTION ( 'NONE',  ( 0.000000000000000000, 1.000000000000000000, -1.471414886128461471E-15 ) ) ;
#214=CARTESIAN_POINT ( 'NONE',  ( 24.55500000000002103, 3.061616997868384620E-16, -2.500000000000001332 ) ) ;
#237=DIRECTION ( 'NONE',  ( 0.000000000000000000, -0.4999999999999993894, 0.8660254037844389297 ) ) ;
#250=AXIS2_PLACEMENT_3D ( 'NONE', #5052, #3664, #1753 ) ;
#256=CARTESIAN_POINT ( 'NONE',  ( 0.000000000000000000, -1.178949249685213863, 2.042000000000002924 ) ) ;
#267=DIRECTION ( 'NONE',  ( 0.000000000000000000, 0.000000000000000000, 1.000000000000000000 ) ) ;
#268=CARTESIAN_POINT ( 'NONE',  ( 0.000000000000000000, -2.357898499370432610, 3.252606517456513302E-15 ) ) ;
#270=ORIENTED_EDGE ( 'NONE', *, *, #6348, .F. ) ;
#290=FACE_OUTER_BOUND ( 'NONE', #6194, .T. ) ;
#297=DIRECTION ( 'NONE',  ( 0.000000000000000000, 0.000000000000000000, -1.000000000000000000 ) ) ;
#313=CARTESIAN_POINT ( 'NONE',  ( 2.500000000000000000, 0.000000000000000000, 0.000000000000000000 ) ) ;
#314=VECTOR ( 'NONE', #3349, 999.9999999999998863 ) ;
#322=VECTOR ( 'NONE', #5585, 1000.000000000000000 ) ;
#330=ORIENTED_EDGE ( 'NONE', *, *, #5204, .F. ) ;
#341=ORIENTED_EDGE ( 'NONE', *, *, #4565, .T. ) ;
#353=FACE_OUTER_BOUND ( 'NONE', #1557, .T. ) ;
#377=DIRECTION ( 'NONE',  ( -1.000000000000000000, -0.000000000000000000, -0.000000000000000000 ) ) ;
#389=CARTESIAN_POINT ( 'NONE',  ( 2.500000000000000000, 1.178949249685213863, -2.042000000000001148 ) ) ;
#399=AXIS2_PLACEMENT_3D ( 'NONE', #8232, #5559, #1521 ) ;
#401=DIRECTION ( 'NONE',  ( -0.000000000000000000, 0.8660254037844390407, 0.4999999999999993339 ) ) ;
#421=FACE_BOUND ( 'NONE', #6148, .T. ) ;
#454=CARTESIAN_POINT ( 'NONE',  ( 2.500000000000000000, 2.500728763858895382E-16, -2.041999999999999815 ) ) ;
#455=CARTESIAN_POINT ( 'NONE',  ( 2.500000000000000000, -1.178949249685213863, 2.042000000000002924 ) ) ;
#456=VECTOR ( 'NONE', #2169, 1000.000000000000000 ) ;
#458=AXIS2_PLACEMENT_3D ( 'NONE', #1269, #3315, #3271 ) ;
#464=DIRECTION ( 'NONE',  ( 0.000000000000000000, 0.000000000000000000, 1.000000000000000000 ) ) ;
#467=EDGE_LOOP ( 'NONE', ( #5929, #7004 ) ) ;
#475=AXIS2_PLACEMENT_3D ( 'NONE', #136, #7508, #2159 ) ;
#483=CARTESIAN_POINT ( 'NONE',  ( 2.500000000000000000, 0.000000000000000000, 0.000000000000000000 ) ) ;
#485=LINE ( 'NONE', #389, #5908 ) ;
#494=DIRECTION ( 'NONE',  ( 0.000000000000000000, 1.000000000000000000, -1.471414886128461471E-15 ) ) ;
#501=ADVANCED_FACE ( 'NONE', ( #3948 ), #5118, .F. ) ;
#513=CARTESIAN_POINT ( 'NONE',  ( 24.55500000000002103, 0.000000000000000000, 0.000000000000000000 ) ) ;
#520=EDGE_LOOP ( 'NONE', ( #4607, #2361, #8228, #5907 ) ) ;
#529=EDGE_LOOP ( 'NONE', ( #8443, #6852, #7945 ) ) ;
#552=ORIENTED_EDGE ( 'NONE', *, *, #6640, .T. ) ;
#577=EDGE_CURVE ( 'NONE', #133, #2563, #1209, .T. ) ;
#591=DIRECTION ( 'NONE',  ( -1.000000000000000000, -0.000000000000000000, -0.000000000000000000 ) ) ;
#594=AXIS2_PLACEMENT_3D ( 'NONE', #3123, #464, #5764 ) ;
#597=ADVANCED_FACE ( 'NONE', ( #5875 ), #3156, .F. ) ;
#612=AXIS2_PLACEMENT_3D ( 'NONE', #910, #7570, #1605 ) ;
#615=CARTESIAN_POINT ( 'NONE',  ( 2.500000000000000000, 0.000000000000000000, 2.041999999999999815 ) ) ;
#622=DIRECTION ( 'NONE',  ( -1.000000000000000000, -0.000000000000000000, -0.000000000000000000 ) ) ;
#629=ADVANCED_FACE ( 'NONE', ( #82 ), #6046, .F. ) ;
#630=SURFACE_STYLE_FILL_AREA ( #7114 ) ;
#664=DIRECTION ( 'NONE',  ( 0.000000000000000000, 0.000000000000000000, -1.000000000000000000 ) ) ;
#671=DIRECTION ( 'NONE',  ( -1.000000000000000000, -0.000000000000000000, -0.000000000000000000 ) ) ;
#736=CIRCLE ( 'NONE', #1858, 2.500000000000000888 ) ;
#739=ORIENTED_EDGE ( 'NONE', *, *, #781, .T. ) ;
#758=EDGE_CURVE ( 'NONE', #2389, #2221, #6961, .T. ) ;
#765=VERTEX_POINT ( 'NONE', #923 ) ;
#781=EDGE_CURVE ( 'NONE', #4350, #1013, #7584, .T. ) ;
#797=CARTESIAN_POINT ( 'NONE',  ( 0.000000000000000000, 0.000000000000000000, 4.000000000000000000 ) ) ;
#798=VERTEX_POINT ( 'NONE', #5567 ) ;
#808=VERTEX_POINT ( 'NONE', #2280 ) ;
#814=FACE_OUTER_BOUND ( 'NONE', #467, .T. ) ;
#826=AXIS2_PLACEMENT_3D ( 'NONE', #2999, #3245, #8556 ) ;
#829=CARTESIAN_POINT ( 'NONE',  ( 24.55500000000002103, 0.000000000000000000, 0.000000000000000000 ) ) ;
#832=VERTEX_POINT ( 'NONE', #214 ) ;
#834=CARTESIAN_POINT ( 'NONE',  ( 0.000000000000000000, 2.357898499370433054, -1.951563910473907981E-15 ) ) ;
#846=CARTESIAN_POINT ( 'NONE',  ( 5.200000000000002842, 3.061616997868384127E-16, -2.500000000000000888 ) ) ;
#848=VERTEX_POINT ( 'NONE', #1578 ) ;
#857=ORIENTED_EDGE ( 'NONE', *, *, #6610, .T. ) ;
#870=ORIENTED_EDGE ( 'NONE', *, *, #6832, .T. ) ;
#879=AXIS2_PLACEMENT_3D ( 'NONE', #1387, #8493, #2531 ) ;
#891=DIRECTION ( 'NONE',  ( 0.000000000000000000, -1.000000000000000000, 1.287488025362403787E-15 ) ) ;
#892=VECTOR ( 'NONE', #2203, 1000.000000000000000 ) ;
#904=CARTESIAN_POINT ( 'NONE',  ( -31.74999999999995737, 3.061616997868384127E-16, -2.500000000000000888 ) ) ;
#906=PRODUCT_CONTEXT ( 'NONE', #5527, 'mechanical' ) ;
#908=ORIENTED_EDGE ( 'NONE', *, *, #5601, .F. ) ;
#910=CARTESIAN_POINT ( 'NONE',  ( 0.2500000000000002220, 0.000000000000000000, 0.000000000000000000 ) ) ;
#915=EDGE_LOOP ( 'NONE', ( #5258, #2722, #7340, #8456, #7652 ) ) ;
#923=CARTESIAN_POINT ( 'NONE',  ( 5.000000000000002665, 0.000000000000000000, -2.700000000000001066 ) ) ;
#933=DIRECTION ( 'NONE',  ( 0.000000000000000000, 0.000000000000000000, 1.000000000000000000 ) ) ;
#934=EDGE_CURVE ( 'NONE', #1995, #7568, #485, .T. ) ;
#961=CARTESIAN_POINT ( 'NONE',  ( 0.000000000000000000, -1.178949249685213863, 2.042000000000002924 ) ) ;
#1007=EDGE_CURVE ( 'NONE', #1337, #765, #4805, .T. ) ;
#1013=VERTEX_POINT ( 'NONE', #1709 ) ;
#1059=AXIS2_PLACEMENT_3D ( 'NONE', #7436, #2132, #1562 ) ;
#1072=ORIENTED_EDGE ( 'NONE', *, *, #5520, .F. ) ;
#1090=EDGE_CURVE ( 'NONE', #5384, #1324, #2588, .T. ) ;
#1105=LINE ( 'NONE', #1146, #3062 ) ;
#1107=VECTOR ( 'NONE', #7729, 1000.000000000000000 ) ;
#1121=ORIENTED_EDGE ( 'NONE', *, *, #2127, .F. ) ;
#1146=CARTESIAN_POINT ( 'NONE',  ( 2.500000000000000000, -1.178949249685213863, 2.042000000000002924 ) ) ;
#1148=ADVANCED_FACE ( 'NONE', ( #4120, #814 ), #4158, .T. ) ;
#1156=VECTOR ( 'NONE', #4836, 999.9999999999998863 ) ;
#1157=VECTOR ( 'NONE', #4825, 999.9999999999998863 ) ;
#1161=( LENGTH_UNIT ( ) NAMED_UNIT ( * ) SI_UNIT ( .MILLI., .METRE. ) );
#1170=DIRECTION ( 'NONE',  ( -1.000000000000000000, -0.000000000000000000, -0.000000000000000000 ) ) ;
#1176=ADVANCED_BREP_SHAPE_REPRESENTATION ( '', ( #1852, #594 ), #5323 ) ;
#1180=AXIS2_PLACEMENT_3D ( 'NONE', #7920, #7259, #5945 ) ;
#1193=CARTESIAN_POINT ( 'NONE',  ( 2.500000000000000000, -1.768423874527823569, 1.021000000000002794 ) ) ;
#1200=ADVANCED_FACE ( 'NONE', ( #290 ), #2827, .F. ) ;
#1209=CIRCLE ( 'NONE', #8452, 0.2500000000000002220 ) ;
#1215=CARTESIAN_POINT ( 'NONE',  ( 0.2500000000000002220, 0.000000000000000000, 0.000000000000000000 ) ) ;
#1220=DIRECTION ( 'NONE',  ( -1.000000000000000000, -0.000000000000000000, -0.000000000000000000 ) ) ;
#1232=DIRECTION ( 'NONE',  ( -0.7071067811865306973, 0.000000000000000000, 0.7071067811865643371 ) ) ;
#1237=EDGE_LOOP ( 'NONE', ( #2489, #3495, #7845, #8047 ) ) ;
#1239=DIRECTION ( 'NONE',  ( 0.000000000000000000, -1.000000000000000000, 1.471414886128461471E-15 ) ) ;
#1250=CIRCLE ( 'NONE', #2379, 0.2500000000000002220 ) ;
#1259=ORIENTED_EDGE ( 'NONE', *, *, #1007, .T. ) ;
#1269=CARTESIAN_POINT ( 'NONE',  ( 2.500000000000000000, 2.357898499370433054, -1.951563910473907981E-15 ) ) ;
#1303=DIRECTION ( 'NONE',  ( 0.000000000000000000, 0.000000000000000000, 1.000000000000000000 ) ) ;
#1305=ORIENTED_EDGE ( 'NONE', *, *, #6099, .F. ) ;
#1312=EDGE_LOOP ( 'NONE', ( #195, #5054, #7974, #2811, #739 ) ) ;
#1321=CARTESIAN_POINT ( 'NONE',  ( 25.00000000000000000, 0.000000000000000000, 2.055000000000000160 ) ) ;
#1324=VERTEX_POINT ( 'NONE', #5645 ) ;
#1328=AXIS2_PLACEMENT_3D ( 'NONE', #513, #7041, #3172 ) ;
#1337=VERTEX_POINT ( 'NONE', #5037 ) ;
#1378=ORIENTED_EDGE ( 'NONE', *, *, #7017, .T. ) ;
#1387=CARTESIAN_POINT ( 'NONE',  ( 25.00000000000000000, 2.055000000000000160, 0.000000000000000000 ) ) ;
#1389=AXIS2_PLACEMENT_3D ( 'NONE', #4237, #6889, #4146 ) ;
#1392=EDGE_CURVE ( 'NONE', #4980, #798, #8360, .T. ) ;
#1395=VECTOR ( 'NONE', #6494, 1000.000000000000000 ) ;
#1410=EDGE_CURVE ( 'NONE', #832, #4980, #4398, .T. ) ;
#1419=DIRECTION ( 'NONE',  ( 0.000000000000000000, 0.000000000000000000, 1.000000000000000000 ) ) ;
#1422=DIRECTION ( 'NONE',  ( 0.000000000000000000, 0.000000000000000000, -1.000000000000000000 ) ) ;
#1430=CARTESIAN_POINT ( 'NONE',  ( -31.74999999999995737, 5.204748896376250699E-16, -4.250000000000000000 ) ) ;
#1438=FACE_OUTER_BOUND ( 'NONE', #2297, .T. ) ;
#1470=CARTESIAN_POINT ( 'NONE',  ( 2.500000000000000000, 0.000000000000000000, 0.000000000000000000 ) ) ;
#1479=SHAPE_REPRESENTATION ( 'socket head cap screw_iso_ISO 4762 M5 x 20 - 20N', ( #594 ), #5323 ) ;
#1488=EDGE_CURVE ( 'NONE', #1985, #2428, #8577, .T. ) ;
#1491=ADVANCED_FACE ( 'NONE', ( #1953 ), #6512, .T. ) ;
#1497=CYLINDRICAL_SURFACE ( 'NONE', #1389, 4.250000000000000000 ) ;
#1509=EDGE_LOOP ( 'NONE', ( #1657, #6, #6723, #2905 ) ) ;
#1521=DIRECTION ( 'NONE',  ( 0.000000000000000000, 0.000000000000000000, 1.000000000000000000 ) ) ;
#1530=AXIS2_PLACEMENT_3D ( 'NONE', #3361, #7276, #664 ) ;
#1535=DIRECTION ( 'NONE',  ( 0.000000000000000000, 0.5000000000000011102, 0.8660254037844380415 ) ) ;
#1538=EDGE_CURVE ( 'NONE', #1967, #3708, #8003, .T. ) ;
#1557=EDGE_LOOP ( 'NONE', ( #1121, #7580, #6490, #5326, #2606 ) ) ;
#1562=DIRECTION ( 'NONE',  ( 0.000000000000000000, 0.000000000000000000, -1.000000000000000000 ) ) ;
#1578=CARTESIAN_POINT ( 'NONE',  ( 2.500000000000000000, 3.004629197474318851E-15, 2.042000000000000259 ) ) ;
#1588=CIRCLE ( 'NONE', #3253, 4.000000000000000000 ) ;
#1592=ORIENTED_EDGE ( 'NONE', *, *, #1759, .F. ) ;
#1596=AXIS2_PLACEMENT_3D ( 'NONE', #4677, #591, #7163 ) ;
#1601=FACE_OUTER_BOUND ( 'NONE', #529, .T. ) ;
#1605=DIRECTION ( 'NONE',  ( 0.000000000000000000, 0.000000000000000000, 1.000000000000000000 ) ) ;
#1614=LINE ( 'NONE', #256, #1882 ) ;
#1617=CARTESIAN_POINT ( 'NONE',  ( 2.500000000000000000, -1.178949249685213863, 2.042000000000002924 ) ) ;
#1618=ADVANCED_FACE ( 'NONE', ( #7466 ), #7738, .T. ) ;
#1637=DIRECTION ( 'NONE',  ( -0.5000000000000051070, 1.060575238724903217E-16, -0.8660254037844355990 ) ) ;
#1657=ORIENTED_EDGE ( 'NONE', *, *, #2296, .T. ) ;
#1685=ORIENTED_EDGE ( 'NONE', *, *, #6878, .T. ) ;
#1709=CARTESIAN_POINT ( 'NONE',  ( 0.000000000000000000, 1.178949249685213863, -2.042000000000001148 ) ) ;
#1726=LINE ( 'NONE', #454, #7000 ) ;
#1731=EDGE_CURVE ( 'NONE', #2415, #6261, #2857, .T. ) ;
#1744=ORIENTED_EDGE ( 'NONE', *, *, #1922, .F. ) ;
#1753=DIRECTION ( 'NONE',  ( 0.000000000000000000, 0.000000000000000000, 1.000000000000000000 ) ) ;
#1759=EDGE_CURVE ( 'NONE', #3580, #1995, #8434, .T. ) ;
#1770=CARTESIAN_POINT ( 'NONE',  ( 0.000000000000000000, 0.000000000000000000, 0.000000000000000000 ) ) ;
#1796=DIRECTION ( 'NONE',  ( 0.000000000000000000, -0.4999999999999993894, 0.8660254037844389297 ) ) ;
#1798=FACE_OUTER_BOUND ( 'NONE', #6425, .T. ) ;
#1818=DIRECTION ( 'NONE',  ( -1.000000000000000000, -0.000000000000000000, -0.000000000000000000 ) ) ;
#1819=EDGE_LOOP ( 'NONE', ( #8004, #6667, #146, #134 ) ) ;
#1834=CARTESIAN_POINT ( 'NONE',  ( 2.500000000000000000, 1.178949249685218525, 2.041999999999999371 ) ) ;
#1852=MANIFOLD_SOLID_BREP ( 'Hex', #7312 ) ;
#1858=AXIS2_PLACEMENT_3D ( 'NONE', #2226, #3573, #297 ) ;
#1859=ADVANCED_FACE ( 'NONE', ( #3370 ), #2048, .T. ) ;
#1863=SURFACE_SIDE_STYLE ('',( #630 ) ) ;
#1882=VECTOR ( 'NONE', #5565, 1000.000000000000114 ) ;
#1888=CARTESIAN_POINT ( 'NONE',  ( 2.500000000000000000, 2.357898499370433054, -1.951563910473907981E-15 ) ) ;
#1920=CARTESIAN_POINT ( 'NONE',  ( 2.500000000000000000, 2.357898499370433054, -1.951563910473907981E-15 ) ) ;
#1922=EDGE_CURVE ( 'NONE', #2428, #1985, #5503, .T. ) ;
#1932=DIRECTION ( 'NONE',  ( 1.000000000000000000, 0.000000000000000000, 0.000000000000000000 ) ) ;
#1953=FACE_OUTER_BOUND ( 'NONE', #5385, .T. ) ;
#1967=VERTEX_POINT ( 'NONE', #7197 ) ;
#1970=CARTESIAN_POINT ( 'NONE',  ( 25.00000000000000000, 2.789133085058098087E-16, -2.055000000000000160 ) ) ;
#1978=DIRECTION ( 'NONE',  ( 0.000000000000000000, 0.000000000000000000, 1.000000000000000000 ) ) ;
#1985=VERTEX_POINT ( 'NONE', #1321 ) ;
#1993=DIRECTION ( 'NONE',  ( 0.000000000000000000, 0.4999999999999993894, -0.8660254037844389297 ) ) ;
#1995=VERTEX_POINT ( 'NONE', #4189 ) ;
#2019=PLANE ( 'NONE',  #1530 ) ;
#2040=DIRECTION ( 'NONE',  ( 0.000000000000000000, 0.4999999999999993339, -0.8660254037844390407 ) ) ;
#2043=CARTESIAN_POINT ( 'NONE',  ( 2.500000000000000000, 0.000000000000000000, 0.000000000000000000 ) ) ;
#2048=CONICAL_SURFACE ( 'NONE', #8307, 2.055000000000000160, 0.7853981633974721488 ) ;
#2080=VERTEX_POINT ( 'NONE', #846 ) ;
#2103=EDGE_CURVE ( 'NONE', #1013, #5774, #2240, .T. ) ;
#2108=ORIENTED_EDGE ( 'NONE', *, *, #2127, .T. ) ;
#2127=EDGE_CURVE ( 'NONE', #3415, #5774, #4453, .T. ) ;
#2132=DIRECTION ( 'NONE',  ( 1.000000000000000000, 0.000000000000000000, 0.000000000000000000 ) ) ;
#2159=DIRECTION ( 'NONE',  ( 0.000000000000000000, 0.000000000000000000, -1.000000000000000000 ) ) ;
#2169=DIRECTION ( 'NONE',  ( -1.000000000000000000, -0.000000000000000000, -0.000000000000000000 ) ) ;
#2170=CARTESIAN_POINT ( 'NONE',  ( 0.000000000000000000, 2.357898499370433054, -1.951563910473907981E-15 ) ) ;
#2171=AXIS2_PLACEMENT_3D ( 'NONE', #3309, #5215, #1303 ) ;
#2199=CARTESIAN_POINT ( 'NONE',  ( 0.000000000000000000, 1.178949249685213863, -2.042000000000001148 ) ) ;
#2203=DIRECTION ( 'NONE',  ( -1.000000000000000000, -0.000000000000000000, -0.000000000000000000 ) ) ;
#2221=VERTEX_POINT ( 'NONE', #1193 ) ;
#2224=ORIENTED_EDGE ( 'NONE', *, *, #758, .F. ) ;
#2226=CARTESIAN_POINT ( 'NONE',  ( 5.200000000000002842, 0.000000000000000000, 0.000000000000000000 ) ) ;
#2240=LINE ( 'NONE', #2199, #2737 ) ;
#2254=DIRECTION ( 'NONE',  ( 0.000000000000000000, 0.000000000000000000, -1.000000000000000000 ) ) ;
#2280=CARTESIAN_POINT ( 'NONE',  ( 3.678949249685231848, 0.000000000000000000, 0.000000000000000000 ) ) ;
#2287=DIRECTION ( 'NONE',  ( 0.000000000000000000, -0.4999999999999992784, 0.8660254037844389297 ) ) ;
#2291=DIRECTION ( 'NONE',  ( 0.000000000000000000, 0.4999999999999993339, -0.8660254037844390407 ) ) ;
#2296=EDGE_CURVE ( 'NONE', #4980, #832, #2754, .T. ) ;
#2297=EDGE_LOOP ( 'NONE', ( #6653, #3730, #6017 ) ) ;
#2312=DIRECTION ( 'NONE',  ( -1.000000000000000000, -0.000000000000000000, -0.000000000000000000 ) ) ;
#2331=ORIENTED_EDGE ( 'NONE', *, *, #7096, .T. ) ;
#2346=EDGE_LOOP ( 'NONE', ( #2224, #7035, #3120 ) ) ;
#2354=DIRECTION ( 'NONE',  ( -1.000000000000000000, 0.000000000000000000, -0.000000000000000000 ) ) ;
#2361=ORIENTED_EDGE ( 'NONE', *, *, #5807, .T. ) ;
#2364=DIRECTION ( 'NONE',  ( 0.000000000000000000, -1.000000000000000000, 1.287488025362403787E-15 ) ) ;
#2373=CARTESIAN_POINT ( 'NONE',  ( 2.500000000000000000, -2.357898499370432610, 3.252606517456513302E-15 ) ) ;
#2378=EDGE_CURVE ( 'NONE', #798, #1337, #8326, .T. ) ;
#2379=AXIS2_PLACEMENT_3D ( 'NONE', #3993, #4590, #2600 ) ;
#2386=LINE ( 'NONE', #3763, #43 ) ;
#2389=VERTEX_POINT ( 'NONE', #8550 ) ;
#2390=( LENGTH_UNIT ( ) NAMED_UNIT ( * ) SI_UNIT ( .MILLI., .METRE. ) );
#2412=AXIS2_PLACEMENT_3D ( 'NONE', #1888, #7058, #4406 ) ;
#2415=VERTEX_POINT ( 'NONE', #7934 ) ;
#2416=TOROIDAL_SURFACE ( 'NONE', #6431, 4.000000000000000000, 0.2500000000000000000 ) ;
#2428=VERTEX_POINT ( 'NONE', #1970 ) ;
#2482=EDGE_LOOP ( 'NONE', ( #6513, #1685, #1592 ) ) ;
#2489=ORIENTED_EDGE ( 'NONE', *, *, #2378, .F. ) ;
#2495=DIRECTION ( 'NONE',  ( 0.000000000000000000, -0.5000000000000011102, -0.8660254037844379305 ) ) ;
#2496=CARTESIAN_POINT ( 'NONE',  ( 0.000000000000000000, 2.357898499370433054, -1.951563910473907981E-15 ) ) ;
#2531=DIRECTION ( 'NONE',  ( 0.000000000000000000, 0.000000000000000000, -1.000000000000000000 ) ) ;
#2540=ORIENTED_EDGE ( 'NONE', *, *, #1410, .F. ) ;
#2561=PRESENTATION_STYLE_ASSIGNMENT (( #5841 ) ) ;
#2563=VERTEX_POINT ( 'NONE', #797 ) ;
#2581=DIRECTION ( 'NONE',  ( -0.5000000000000051070, 0.000000000000000000, 0.8660254037844355990 ) ) ;
#2582=CARTESIAN_POINT ( 'NONE',  ( 5.200000000000002842, 0.000000000000000000, 0.000000000000000000 ) ) ;
#2588=CIRCLE ( 'NONE', #2171, 4.250000000000000000 ) ;
#2600=DIRECTION ( 'NONE',  ( 0.000000000000000000, -1.224646799147353454E-16, 1.000000000000000000 ) ) ;
#2602=VECTOR ( 'NONE', #2291, 1000.000000000000000 ) ;
#2604=AXIS2_PLACEMENT_3D ( 'NONE', #7359, #7319, #7403 ) ;
#2606=ORIENTED_EDGE ( 'NONE', *, *, #4298, .T. ) ;
#2645=CONICAL_SURFACE ( 'NONE', #7364, 2.041999999999999815, 1.047197551196591858 ) ;
#2679=ORIENTED_EDGE ( 'NONE', *, *, #6640, .F. ) ;
#2681=ORIENTED_EDGE ( 'NONE', *, *, #577, .T. ) ;
#2686=VECTOR ( 'NONE', #5471, 1000.000000000000000 ) ;
#2692=ADVANCED_FACE ( 'NONE', ( #1798 ), #3792, .T. ) ;
#2708=ORIENTED_EDGE ( 'NONE', *, *, #2378, .T. ) ;
#2714=DIRECTION ( 'NONE',  ( 0.000000000000000000, 1.224646799147353207E-16, 1.000000000000000000 ) ) ;
#2722=ORIENTED_EDGE ( 'NONE', *, *, #6366, .F. ) ;
#2723=VECTOR ( 'NONE', #1170, 1000.000000000000000 ) ;
#2737=VECTOR ( 'NONE', #891, 1000.000000000000000 ) ;
#2738=CARTESIAN_POINT ( 'NONE',  ( 25.00000000000000000, 0.000000000000000000, 0.000000000000000000 ) ) ;
#2751=LINE ( 'NONE', #615, #6570 ) ;
#2754=CIRCLE ( 'NONE', #3307, 2.500000000000001332 ) ;
#2782=LINE ( 'NONE', #2170, #1157 ) ;
#2786=ORIENTED_EDGE ( 'NONE', *, *, #3139, .F. ) ;
#2811=ORIENTED_EDGE ( 'NONE', *, *, #6878, .F. ) ;
#2824=VECTOR ( 'NONE', #4081, 1000.000000000000000 ) ;
#2827=PLANE ( 'NONE',  #1059 ) ;
#2835=CARTESIAN_POINT ( 'NONE',  ( 5.000000000000004441, 0.000000000000000000, 4.250000000000000000 ) ) ;
#2854=CARTESIAN_POINT ( 'NONE',  ( 2.500000000000000000, -1.178949249685213863, 2.042000000000002924 ) ) ;
#2857=LINE ( 'NONE', #6202, #5911 ) ;
#2859=CARTESIAN_POINT ( 'NONE',  ( 5.000000000000000888, 4.250000000000000000, 0.000000000000000000 ) ) ;
#2892=EDGE_CURVE ( 'NONE', #3708, #2221, #4154, .T. ) ;
#2905=ORIENTED_EDGE ( 'NONE', *, *, #1392, .F. ) ;
#2923=ORIENTED_EDGE ( 'NONE', *, *, #1488, .T. ) ;
#2931=LINE ( 'NONE', #5147, #1107 ) ;
#2940=CARTESIAN_POINT ( 'NONE',  ( 0.2500000000000002220, 0.000000000000000000, 0.000000000000000000 ) ) ;
#2945=UNCERTAINTY_MEASURE_WITH_UNIT (LENGTH_MEASURE( 1.000000000000000082E-05 ), #2390, 'distance_accuracy_value', 'NONE');
#2955=EDGE_CURVE ( 'NONE', #2563, #5355, #4432, .T. ) ;
#2977=CIRCLE ( 'NONE', #612, 4.250000000000000000 ) ;
#2999=CARTESIAN_POINT ( 'NONE',  ( 5.200000000000002842, 0.000000000000000000, -2.700000000000001066 ) ) ;
#3013=AXIS2_PLACEMENT_3D ( 'NONE', #2043, #3429, #4687 ) ;
#3016=CARTESIAN_POINT ( 'NONE',  ( -31.74999999999995737, 0.000000000000000000, 0.000000000000000000 ) ) ;
#3021=PLANE ( 'NONE',  #27 ) ;
#3052=ORIENTED_EDGE ( 'NONE', *, *, #5331, .F. ) ;
#3062=VECTOR ( 'NONE', #494, 1000.000000000000000 ) ;
#3063=PLANE ( 'NONE',  #5587 ) ;
#3067=CONICAL_SURFACE ( 'NONE', #6397, 2.041999999999999815, 1.047197551196591858 ) ;
#3077=ORIENTED_EDGE ( 'NONE', *, *, #3420, .T. ) ;
#3093=CARTESIAN_POINT ( 'NONE',  ( 2.500000000000000000, -1.178949249685213863, 2.042000000000002924 ) ) ;
#3112=EDGE_LOOP ( 'NONE', ( #2679, #8402, #5950, #4395, #3077 ) ) ;
#3120=ORIENTED_EDGE ( 'NONE', *, *, #7017, .F. ) ;
#3123=CARTESIAN_POINT ( 'NONE',  ( 0.000000000000000000, 0.000000000000000000, 0.000000000000000000 ) ) ;
#3139=EDGE_CURVE ( 'NONE', #2080, #765, #6236, .T. ) ;
#3155=STYLED_ITEM('',(#8671),#1852);
#3156=TOROIDAL_SURFACE ( 'NONE', #3436, 2.700000000000001066, 0.2000000000000000111 ) ;
#3172=DIRECTION ( 'NONE',  ( 0.000000000000000000, 0.000000000000000000, 1.000000000000000000 ) ) ;
#3205=CARTESIAN_POINT ( 'NONE',  ( 25.00000000000000000, 0.000000000000000000, 0.000000000000000000 ) ) ;
#3225=PRODUCT_DEFINITION_SHAPE ( 'NONE', 'NONE',  #6591 ) ;
#3226=DIRECTION ( 'NONE',  ( -1.000000000000000000, -0.000000000000000000, -0.000000000000000000 ) ) ;
#3233=AXIS2_PLACEMENT_3D ( 'NONE', #1215, #3873, #3260 ) ;
#3240=CARTESIAN_POINT ( 'NONE',  ( 2.500000000000000000, 2.357898499370433054, -1.951563910473907981E-15 ) ) ;
#3245=DIRECTION ( 'NONE',  ( 0.000000000000000000, -1.000000000000000000, 0.000000000000000000 ) ) ;
#3253=AXIS2_PLACEMENT_3D ( 'NONE', #1770, #622, #6581 ) ;
#3260=DIRECTION ( 'NONE',  ( 0.000000000000000000, 0.000000000000000000, 1.000000000000000000 ) ) ;
#3271=DIRECTION ( 'NONE',  ( 0.000000000000000000, 0.000000000000000000, -1.000000000000000000 ) ) ;
#3276=ORIENTED_EDGE ( 'NONE', *, *, #1410, .T. ) ;
#3277=CARTESIAN_POINT ( 'NONE',  ( 2.500000000000000000, -1.768423874527823791, -1.020999999999998353 ) ) ;
#3305=LINE ( 'NONE', #1920, #314 ) ;
#3307=AXIS2_PLACEMENT_3D ( 'NONE', #829, #5479, #4832 ) ;
#3309=CARTESIAN_POINT ( 'NONE',  ( 5.000000000000004441, 0.000000000000000000, 0.000000000000000000 ) ) ;
#3315=DIRECTION ( 'NONE',  ( 1.000000000000000000, 0.000000000000000000, 0.000000000000000000 ) ) ;
#3318=CARTESIAN_POINT ( 'NONE',  ( 5.200000000000002842, 3.306546357697854719E-16, 2.700000000000001066 ) ) ;
#3333=ORIENTED_EDGE ( 'NONE', *, *, #6034, .F. ) ;
#3339=CARTESIAN_POINT ( 'NONE',  ( 2.500000000000000000, -2.357898499370432610, 3.252606517456513302E-15 ) ) ;
#3349=DIRECTION ( 'NONE',  ( 0.000000000000000000, -0.5000000000000012212, -0.8660254037844380415 ) ) ;
#3361=CARTESIAN_POINT ( 'NONE',  ( 2.500000000000000000, 2.357898499370433054, -1.951563910473907981E-15 ) ) ;
#3365=CARTESIAN_POINT ( 'NONE',  ( 5.200000000000002842, 0.000000000000000000, 0.000000000000000000 ) ) ;
#3370=FACE_OUTER_BOUND ( 'NONE', #4211, .T. ) ;
#3372=( NAMED_UNIT ( * ) SI_UNIT ( $, .STERADIAN. ) SOLID_ANGLE_UNIT ( ) );
#3376=UNCERTAINTY_MEASURE_WITH_UNIT (LENGTH_MEASURE( 1.000000000000000082E-05 ), #1161, 'distance_accuracy_value', 'NONE');
#3377=ORIENTED_EDGE ( 'NONE', *, *, #7932, .F. ) ;
#3393=MECHANICAL_DESIGN_GEOMETRIC_PRESENTATION_REPRESENTATION('',(#8534),#4772);
#3394=PLANE ( 'NONE',  #879 ) ;
#3411=CARTESIAN_POINT ( 'NONE',  ( 25.00000000000000000, 2.516649172247811061E-16, -2.055000000000000160 ) ) ;
#3415=VERTEX_POINT ( 'NONE', #268 ) ;
#3420=EDGE_CURVE ( 'NONE', #1967, #3415, #2931, .T. ) ;
#3429=DIRECTION ( 'NONE',  ( -1.000000000000000000, -0.000000000000000000, -0.000000000000000000 ) ) ;
#3436=AXIS2_PLACEMENT_3D ( 'NONE', #2582, #1932, #7101 ) ;
#3464=CARTESIAN_POINT ( 'NONE',  ( 2.500000000000000000, 1.768423874527824902, 1.020999999999999019 ) ) ;
#3490=CARTESIAN_POINT ( 'NONE',  ( 2.500000000000000000, 2.357898499370433054, -1.951563910473907981E-15 ) ) ;
#3491=EDGE_CURVE ( 'NONE', #2389, #848, #1105, .T. ) ;
#3495=ORIENTED_EDGE ( 'NONE', *, *, #5359, .F. ) ;
#3497=CARTESIAN_POINT ( 'NONE',  ( 24.55500000000002103, 0.000000000000000000, 2.500000000000001332 ) ) ;
#3559=CARTESIAN_POINT ( 'NONE',  ( 0.000000000000000000, -1.178949249685218303, -2.041999999999998039 ) ) ;
#3573=DIRECTION ( 'NONE',  ( 1.000000000000000000, 0.000000000000000000, 0.000000000000000000 ) ) ;
#3580=VERTEX_POINT ( 'NONE', #5310 ) ;
#3614=ORIENTED_EDGE ( 'NONE', *, *, #6832, .F. ) ;
#3615=LINE ( 'NONE', #6124, #1156 ) ;
#3643=CARTESIAN_POINT ( 'NONE',  ( 0.000000000000000000, 0.000000000000000000, 0.000000000000000000 ) ) ;
#3664=DIRECTION ( 'NONE',  ( -1.000000000000000000, -0.000000000000000000, -0.000000000000000000 ) ) ;
#3673=ADVANCED_FACE ( 'NONE', ( #4710 ), #2019, .F. ) ;
#3691=DIRECTION ( 'NONE',  ( -0.000000000000000000, 0.000000000000000000, 1.000000000000000000 ) ) ;
#3708=VERTEX_POINT ( 'NONE', #3277 ) ;
#3725=DIRECTION ( 'NONE',  ( 0.000000000000000000, 0.000000000000000000, 1.000000000000000000 ) ) ;
#3730=ORIENTED_EDGE ( 'NONE', *, *, #7179, .F. ) ;
#3757=CARTESIAN_POINT ( 'NONE',  ( 2.500000000000000000, -1.178949249685218303, -2.041999999999998039 ) ) ;
#3763=CARTESIAN_POINT ( 'NONE',  ( 2.500000000000000000, 1.178949249685218525, 2.041999999999999371 ) ) ;
#3770=ADVANCED_FACE ( 'NONE', ( #7449 ), #7630, .T. ) ;
#3786=CIRCLE ( 'NONE', #3233, 4.250000000000000000 ) ;
#3792=CYLINDRICAL_SURFACE ( 'NONE', #250, 4.250000000000000000 ) ;
#3797=FACE_OUTER_BOUND ( 'NONE', #2346, .T. ) ;
#3836=ADVANCED_FACE ( 'NONE', ( #6357 ), #7012, .T. ) ;
#3841=EDGE_LOOP ( 'NONE', ( #2923, #8157, #4049, #5856 ) ) ;
#3870=EDGE_LOOP ( 'NONE', ( #4110, #5610, #908, #3052, #857 ) ) ;
#3873=DIRECTION ( 'NONE',  ( 1.000000000000000000, 0.000000000000000000, 0.000000000000000000 ) ) ;
#3874=ORIENTED_EDGE ( 'NONE', *, *, #6909, .T. ) ;
#3932=CONICAL_SURFACE ( 'NONE', #163, 2.055000000000000160, 0.7853981633974721488 ) ;
#3948=FACE_OUTER_BOUND ( 'NONE', #915, .T. ) ;
#3993=CARTESIAN_POINT ( 'NONE',  ( 0.2500000000000002220, 4.898587196589412829E-16, -4.000000000000000000 ) ) ;
#3997=CARTESIAN_POINT ( 'NONE',  ( 2.500000000000000000, 2.357898499370433054, -1.951563910473907981E-15 ) ) ;
#4018=ADVANCED_FACE ( 'NONE', ( #180 ), #2645, .F. ) ;
#4023=AXIS2_PLACEMENT_3D ( 'NONE', #6182, #6792, #1535 ) ;
#4049=ORIENTED_EDGE ( 'NONE', *, *, #2296, .F. ) ;
#4076=VECTOR ( 'NONE', #6806, 1000.000000000000000 ) ;
#4081=DIRECTION ( 'NONE',  ( -1.000000000000000000, -0.000000000000000000, -0.000000000000000000 ) ) ;
#4092=AXIS2_PLACEMENT_3D ( 'NONE', #483, #7797, #4479 ) ;
#4097=DIRECTION ( 'NONE',  ( 0.000000000000000000, 0.000000000000000000, -1.000000000000000000 ) ) ;
#4110=ORIENTED_EDGE ( 'NONE', *, *, #7218, .T. ) ;
#4117=ORIENTED_EDGE ( 'NONE', *, *, #6034, .T. ) ;
#4120=FACE_BOUND ( 'NONE', #5672, .T. ) ;
#4129=ADVANCED_FACE ( 'NONE', ( #6232 ), #3067, .F. ) ;
#4146=DIRECTION ( 'NONE',  ( 0.000000000000000000, 0.000000000000000000, 1.000000000000000000 ) ) ;
#4154=CIRCLE ( 'NONE', #7209, 2.041999999999999815 ) ;
#4158=PLANE ( 'NONE',  #7973 ) ;
#4169=ADVANCED_FACE ( 'NONE', ( #4888 ), #1497, .T. ) ;
#4186=APPLICATION_CONTEXT ( 'automotive_design' ) ;
#4189=CARTESIAN_POINT ( 'NONE',  ( 2.500000000000000000, -2.629050547790028551E-15, -2.041999999999999815 ) ) ;
#4190=PRODUCT_DEFINITION_FORMATION_WITH_SPECIFIED_SOURCE ( 'ANY', '', #6621, .NOT_KNOWN. ) ;
#4198=CARTESIAN_POINT ( 'NONE',  ( 2.500000000000000000, -1.178949249685218303, -2.041999999999998039 ) ) ;
#4211=EDGE_LOOP ( 'NONE', ( #7619, #5605, #4671, #2540 ) ) ;
#4233=CIRCLE ( 'NONE', #188, 2.041999999999999815 ) ;
#4237=CARTESIAN_POINT ( 'NONE',  ( -31.74999999999995737, 0.000000000000000000, 0.000000000000000000 ) ) ;
#4263=AXIS2_PLACEMENT_3D ( 'NONE', #3205, #5275, #7944 ) ;
#4283=EDGE_LOOP ( 'NONE', ( #1305, #5498, #2681, #6760 ) ) ;
#4298=EDGE_CURVE ( 'NONE', #7568, #5774, #8381, .T. ) ;
#4336=ORIENTED_EDGE ( 'NONE', *, *, #4872, .T. ) ;
#4350=VERTEX_POINT ( 'NONE', #5693 ) ;
#4354=VECTOR ( 'NONE', #2495, 1000.000000000000114 ) ;
#4378=CIRCLE ( 'NONE', #1596, 2.700000000000001066 ) ;
#4395=ORIENTED_EDGE ( 'NONE', *, *, #5520, .T. ) ;
#4398=CIRCLE ( 'NONE', #1328, 2.500000000000001332 ) ;
#4406=DIRECTION ( 'NONE',  ( 0.000000000000000000, 0.000000000000000000, -1.000000000000000000 ) ) ;
#4415=DIRECTION ( 'NONE',  ( 1.000000000000000000, 0.000000000000000000, 0.000000000000000000 ) ) ;
#4432=CIRCLE ( 'NONE', #399, 4.000000000000000000 ) ;
#4446=VERTEX_POINT ( 'NONE', #961 ) ;
#4453=LINE ( 'NONE', #5577, #2602 ) ;
#4479=DIRECTION ( 'NONE',  ( 0.000000000000000000, 0.000000000000000000, 1.000000000000000000 ) ) ;
#4487=FACE_OUTER_BOUND ( 'NONE', #1312, .T. ) ;
#4497=COLOUR_RGB ( '',1.000000000000000000, 0.9490196078431372140, 0.9098039215686274384 ) ;
#4501=CARTESIAN_POINT ( 'NONE',  ( 25.00000000000000000, 0.000000000000000000, 2.055000000000000160 ) ) ;
#4504=( NAMED_UNIT ( * ) SI_UNIT ( $, .STERADIAN. ) SOLID_ANGLE_UNIT ( ) );
#4507=CIRCLE ( 'NONE', #4092, 2.041999999999999815 ) ;
#4525=PLANE ( 'NONE',  #2412 ) ;
#4528=CARTESIAN_POINT ( 'NONE',  ( 0.2500000000000002220, 0.000000000000000000, 4.000000000000000000 ) ) ;
#4543=( NAMED_UNIT ( * ) PLANE_ANGLE_UNIT ( ) SI_UNIT ( $, .RADIAN. ) );
#4544=CARTESIAN_POINT ( 'NONE',  ( 2.500000000000000000, -1.178949249685213863, 2.042000000000002924 ) ) ;
#4557=CARTESIAN_POINT ( 'NONE',  ( 5.000000000000004441, 0.000000000000000000, 0.000000000000000000 ) ) ;
#4565=EDGE_CURVE ( 'NONE', #133, #8215, #3786, .T. ) ;
#4585=FILL_AREA_STYLE_COLOUR ( '', #4497 ) ;
#4590=DIRECTION ( 'NONE',  ( -0.000000000000000000, 1.000000000000000000, 1.224646799147353207E-16 ) ) ;
#4607=ORIENTED_EDGE ( 'NONE', *, *, #1090, .T. ) ;
#4621=AXIS2_PLACEMENT_3D ( 'NONE', #4917, #7442, #4097 ) ;
#4671=ORIENTED_EDGE ( 'NONE', *, *, #7823, .T. ) ;
#4677=CARTESIAN_POINT ( 'NONE',  ( 5.000000000000000888, 0.000000000000000000, 0.000000000000000000 ) ) ;
#4687=DIRECTION ( 'NONE',  ( 0.000000000000000000, 0.000000000000000000, 1.000000000000000000 ) ) ;
#4710=FACE_OUTER_BOUND ( 'NONE', #2482, .T. ) ;
#4720=ORIENTED_EDGE ( 'NONE', *, *, #1538, .F. ) ;
#4738=ADVANCED_FACE ( 'NONE', ( #1601 ), #7193, .F. ) ;
#4740=DIRECTION ( 'NONE',  ( 0.000000000000000000, 0.000000000000000000, 1.000000000000000000 ) ) ;
#4756=VECTOR ( 'NONE', #6797, 1000.000000000000000 ) ;
#4770=LINE ( 'NONE', #7422, #4076 ) ;
#4772=( GEOMETRIC_REPRESENTATION_CONTEXT ( 3 ) GLOBAL_UNCERTAINTY_ASSIGNED_CONTEXT ( ( #3376 ) ) GLOBAL_UNIT_ASSIGNED_CONTEXT ( ( #1161, #7496, #3372 ) ) REPRESENTATION_CONTEXT ( 'NONE', 'WORKASPACE' ) );
#4784=CIRCLE ( 'NONE', #1180, 2.041999999999999815 ) ;
#4805=CIRCLE ( 'NONE', #6888, 2.700000000000001066 ) ;
#4806=ORIENTED_EDGE ( 'NONE', *, *, #7932, .T. ) ;
#4825=DIRECTION ( 'NONE',  ( 0.000000000000000000, -0.5000000000000012212, -0.8660254037844380415 ) ) ;
#4832=DIRECTION ( 'NONE',  ( 0.000000000000000000, 0.000000000000000000, 1.000000000000000000 ) ) ;
#4836=DIRECTION ( 'NONE',  ( 0.000000000000000000, -0.5000000000000012212, -0.8660254037844380415 ) ) ;
#4847=DIRECTION ( 'NONE',  ( 0.000000000000000000, 0.000000000000000000, -1.000000000000000000 ) ) ;
#4848=DIRECTION ( 'NONE',  ( -1.000000000000000000, -0.000000000000000000, -0.000000000000000000 ) ) ;
#4872=EDGE_CURVE ( 'NONE', #6261, #6900, #6924, .T. ) ;
#4888=FACE_OUTER_BOUND ( 'NONE', #520, .T. ) ;
#4900=AXIS2_PLACEMENT_3D ( 'NONE', #3365, #6010, #4847 ) ;
#4906=AXIS2_PLACEMENT_3D ( 'NONE', #4557, #8578, #7876 ) ;
#4917=CARTESIAN_POINT ( 'NONE',  ( 2.500000000000000000, 2.357898499370433054, -1.951563910473907981E-15 ) ) ;
#4955=CIRCLE ( 'NONE', #3013, 2.041999999999999815 ) ;
#4974=DIRECTION ( 'NONE',  ( 0.000000000000000000, -0.4999999999999993894, 0.8660254037844389297 ) ) ;
#4978=DIRECTION ( 'NONE',  ( -1.000000000000000000, -0.000000000000000000, -0.000000000000000000 ) ) ;
#4980=VERTEX_POINT ( 'NONE', #3497 ) ;
#4985=ORIENTED_EDGE ( 'NONE', *, *, #1731, .F. ) ;
#4990=FACE_OUTER_BOUND ( 'NONE', #8344, .T. ) ;
#5026=( NAMED_UNIT ( * ) PLANE_ANGLE_UNIT ( ) SI_UNIT ( $, .RADIAN. ) );
#5037=CARTESIAN_POINT ( 'NONE',  ( 5.000000000000002665, 3.306546357697854226E-16, 2.700000000000001066 ) ) ;
#5052=CARTESIAN_POINT ( 'NONE',  ( -31.74999999999995737, 0.000000000000000000, 0.000000000000000000 ) ) ;
#5054=ORIENTED_EDGE ( 'NONE', *, *, #4298, .F. ) ;
#5056=TOROIDAL_SURFACE ( 'NONE', #475, 2.700000000000001066, 0.2000000000000000111 ) ;
#5087=VECTOR ( 'NONE', #2040, 1000.000000000000000 ) ;
#5100=ADVANCED_FACE ( 'NONE', ( #4487 ), #3063, .F. ) ;
#5101=DIRECTION ( 'NONE',  ( 0.000000000000000000, -1.000000000000000000, 0.000000000000000000 ) ) ;
#5118=PLANE ( 'NONE',  #7182 ) ;
#5119=ORIENTED_EDGE ( 'NONE', *, *, #7096, .F. ) ;
#5139=ADVANCED_FACE ( 'NONE', ( #3797 ), #4525, .F. ) ;
#5147=CARTESIAN_POINT ( 'NONE',  ( 2.500000000000000000, -2.357898499370432610, 3.252606517456513302E-15 ) ) ;
#5153=CARTESIAN_POINT ( 'NONE',  ( 25.00000000000000000, 0.000000000000000000, 0.000000000000000000 ) ) ;
#5194=VECTOR ( 'NONE', #212, 1000.000000000000000 ) ;
#5204=EDGE_CURVE ( 'NONE', #808, #848, #2751, .T. ) ;
#5208=ADVANCED_FACE ( 'NONE', ( #8588 ), #6696, .F. ) ;
#5215=DIRECTION ( 'NONE',  ( -1.000000000000000000, -0.000000000000000000, -0.000000000000000000 ) ) ;
#5243=PRODUCT_DEFINITION_CONTEXT ( 'detailed design', #4186, 'design' ) ;
#5258=ORIENTED_EDGE ( 'NONE', *, *, #6651, .T. ) ;
#5271=CARTESIAN_POINT ( 'NONE',  ( 0.2500000000000002220, 0.000000000000000000, 0.000000000000000000 ) ) ;
#5275=DIRECTION ( 'NONE',  ( -1.000000000000000000, -0.000000000000000000, -0.000000000000000000 ) ) ;
#5310=CARTESIAN_POINT ( 'NONE',  ( 2.500000000000000000, 1.768423874527822681, -1.021000000000002794 ) ) ;
#5323=( GEOMETRIC_REPRESENTATION_CONTEXT ( 3 ) GLOBAL_UNCERTAINTY_ASSIGNED_CONTEXT ( ( #5371 ) ) GLOBAL_UNIT_ASSIGNED_CONTEXT ( ( #5973, #4543, #4504 ) ) REPRESENTATION_CONTEXT ( 'NONE', 'WORKASPACE' ) );
#5326=ORIENTED_EDGE ( 'NONE', *, *, #7179, .T. ) ;
#5331=EDGE_CURVE ( 'NONE', #2415, #3580, #3615, .T. ) ;
#5355=VERTEX_POINT ( 'NONE', #5484 ) ;
#5358=AXIS2_PLACEMENT_3D ( 'NONE', #7910, #6023, #1419 ) ;
#5359=EDGE_CURVE ( 'NONE', #2080, #798, #736, .T. ) ;
#5371=UNCERTAINTY_MEASURE_WITH_UNIT (LENGTH_MEASURE( 1.000000000000000082E-05 ), #5973, 'distance_accuracy_value', 'NONE');
#5381=CARTESIAN_POINT ( 'NONE',  ( 0.2500000000000002220, 0.000000000000000000, 4.250000000000000000 ) ) ;
#5384=VERTEX_POINT ( 'NONE', #2835 ) ;
#5385=EDGE_LOOP ( 'NONE', ( #3614, #5761, #8201, #4336, #8455 ) ) ;
#5471=DIRECTION ( 'NONE',  ( 0.000000000000000000, 0.4999999999999993339, -0.8660254037844390407 ) ) ;
#5479=DIRECTION ( 'NONE',  ( -1.000000000000000000, -0.000000000000000000, -0.000000000000000000 ) ) ;
#5484=CARTESIAN_POINT ( 'NONE',  ( 0.000000000000000000, 5.051668046482832750E-16, -4.000000000000000000 ) ) ;
#5485=LINE ( 'NONE', #6661, #5194 ) ;
#5490=SHAPE_REPRESENTATION_RELATIONSHIP ( 'NONE' , 'NONE' ,  #1479, #1176 ) ;
#5491=CARTESIAN_POINT ( 'NONE',  ( 2.500000000000000000, 2.357898499370433054, -1.951563910473907981E-15 ) ) ;
#5493=AXIS2_PLACEMENT_3D ( 'NONE', #3643, #2354, #3691 ) ;
#5498=ORIENTED_EDGE ( 'NONE', *, *, #4565, .F. ) ;
#5503=CIRCLE ( 'NONE', #4263, 2.055000000000000160 ) ;
#5520=EDGE_CURVE ( 'NONE', #2221, #1967, #6349, .T. ) ;
#5525=AXIS2_PLACEMENT_3D ( 'NONE', #3318, #83, #2714 ) ;
#5527=APPLICATION_CONTEXT ( 'automotive_design' ) ;
#5559=DIRECTION ( 'NONE',  ( -1.000000000000000000, -0.000000000000000000, -0.000000000000000000 ) ) ;
#5565=DIRECTION ( 'NONE',  ( 0.000000000000000000, -0.5000000000000011102, -0.8660254037844379305 ) ) ;
#5567=CARTESIAN_POINT ( 'NONE',  ( 5.200000000000002842, 0.000000000000000000, 2.500000000000000888 ) ) ;
#5577=CARTESIAN_POINT ( 'NONE',  ( 0.000000000000000000, -2.357898499370432610, 3.252606517456513302E-15 ) ) ;
#5582=ORIENTED_EDGE ( 'NONE', *, *, #6651, .F. ) ;
#5585=DIRECTION ( 'NONE',  ( 0.000000000000000000, 1.000000000000000000, -1.471414886128461471E-15 ) ) ;
#5587=AXIS2_PLACEMENT_3D ( 'NONE', #7145, #6491, #7765 ) ;
#5600=DIRECTION ( 'NONE',  ( 0.000000000000000000, 0.000000000000000000, 1.000000000000000000 ) ) ;
#5601=EDGE_CURVE ( 'NONE', #3580, #4350, #3305, .T. ) ;
#5602=EDGE_CURVE ( 'NONE', #1324, #5384, #7261, .T. ) ;
#5605=ORIENTED_EDGE ( 'NONE', *, *, #1922, .T. ) ;
#5610=ORIENTED_EDGE ( 'NONE', *, *, #781, .F. ) ;
#5620=VECTOR ( 'NONE', #2364, 1000.000000000000000 ) ;
#5628=ADVANCED_FACE ( 'NONE', ( #6556 ), #3394, .T. ) ;
#5630=ORIENTED_EDGE ( 'NONE', *, *, #2892, .F. ) ;
#5645=CARTESIAN_POINT ( 'NONE',  ( 5.000000000000004441, 5.204748896376250699E-16, -4.250000000000000000 ) ) ;
#5656=LINE ( 'NONE', #8458, #5620 ) ;
#5657=DIRECTION ( 'NONE',  ( 0.000000000000000000, -0.5000000000000011102, -0.8660254037844379305 ) ) ;
#5672=EDGE_LOOP ( 'NONE', ( #4117, #1259 ) ) ;
#5680=ORIENTED_EDGE ( 'NONE', *, *, #2892, .T. ) ;
#5685=DIRECTION ( 'NONE',  ( 0.000000000000000000, 0.000000000000000000, 1.000000000000000000 ) ) ;
#5693=CARTESIAN_POINT ( 'NONE',  ( 2.500000000000000000, 1.178949249685213863, -2.042000000000001148 ) ) ;
#5738=EDGE_CURVE ( 'NONE', #8215, #133, #2977, .T. ) ;
#5743=DIRECTION ( 'NONE',  ( 0.000000000000000000, -1.000000000000000000, 1.287488025362403787E-15 ) ) ;
#5760=ADVANCED_FACE ( 'NONE', ( #6733 ), #3932, .T. ) ;
#5761=ORIENTED_EDGE ( 'NONE', *, *, #6610, .F. ) ;
#5764=DIRECTION ( 'NONE',  ( 1.000000000000000000, 0.000000000000000000, 0.000000000000000000 ) ) ;
#5774=VERTEX_POINT ( 'NONE', #3559 ) ;
#5807=EDGE_CURVE ( 'NONE', #1324, #8215, #6905, .T. ) ;
#5835=DIRECTION ( 'NONE',  ( -1.000000000000000000, -0.000000000000000000, -0.000000000000000000 ) ) ;
#5841=SURFACE_STYLE_USAGE ( .BOTH. , #1863 ) ;
#5850=VERTEX_POINT ( 'NONE', #6211 ) ;
#5856=ORIENTED_EDGE ( 'NONE', *, *, #7823, .F. ) ;
#5857=AXIS2_PLACEMENT_3D ( 'NONE', #3240, #4415, #2254 ) ;
#5861=VECTOR ( 'NONE', #1232, 1000.000000000000000 ) ;
#5866=DIRECTION ( 'NONE',  ( 0.000000000000000000, 0.000000000000000000, -1.000000000000000000 ) ) ;
#5875=FACE_OUTER_BOUND ( 'NONE', #205, .T. ) ;
#5894=AXIS2_PLACEMENT_3D ( 'NONE', #7659, #377, #5685 ) ;
#5907=ORIENTED_EDGE ( 'NONE', *, *, #7554, .F. ) ;
#5908=VECTOR ( 'NONE', #5743, 1000.000000000000000 ) ;
#5911=VECTOR ( 'NONE', #237, 1000.000000000000114 ) ;
#5929=ORIENTED_EDGE ( 'NONE', *, *, #1090, .F. ) ;
#5945=DIRECTION ( 'NONE',  ( 0.000000000000000000, 0.000000000000000000, 1.000000000000000000 ) ) ;
#5950=ORIENTED_EDGE ( 'NONE', *, *, #758, .T. ) ;
#5965=ADVANCED_FACE ( 'NONE', ( #421, #6992 ), #6949, .T. ) ;
#5967=ADVANCED_FACE ( 'NONE', ( #4990 ), #6336, .T. ) ;
#5972=EDGE_LOOP ( 'NONE', ( #6816, #1744 ) ) ;
#5973=( LENGTH_UNIT ( ) NAMED_UNIT ( * ) SI_UNIT ( .MILLI., .METRE. ) );
#6010=DIRECTION ( 'NONE',  ( 1.000000000000000000, 0.000000000000000000, 0.000000000000000000 ) ) ;
#6014=DIRECTION ( 'NONE',  ( 0.000000000000000000, 0.000000000000000000, 1.000000000000000000 ) ) ;
#6017=ORIENTED_EDGE ( 'NONE', *, *, #6909, .F. ) ;
#6023=DIRECTION ( 'NONE',  ( -1.000000000000000000, -0.000000000000000000, -0.000000000000000000 ) ) ;
#6034=EDGE_CURVE ( 'NONE', #765, #1337, #4378, .T. ) ;
#6046=PLANE ( 'NONE',  #2604 ) ;
#6068=LINE ( 'NONE', #904, #2824 ) ;
#6099=EDGE_CURVE ( 'NONE', #8215, #5355, #1250, .T. ) ;
#6107=EDGE_LOOP ( 'NONE', ( #330, #7221, #3874, #5680, #1378 ) ) ;
#6124=CARTESIAN_POINT ( 'NONE',  ( 2.500000000000000000, 2.357898499370433054, -1.951563910473907981E-15 ) ) ;
#6128=EDGE_CURVE ( 'NONE', #2389, #4446, #7377, .T. ) ;
#6148=EDGE_LOOP ( 'NONE', ( #870, #5582, #552, #2108, #7629, #6864 ) ) ;
#6155=ADVANCED_FACE ( 'NONE', ( #7338 ), #5056, .F. ) ;
#6182=CARTESIAN_POINT ( 'NONE',  ( 2.500000000000000000, -1.178949249685213863, 2.042000000000002924 ) ) ;
#6194=EDGE_LOOP ( 'NONE', ( #4985, #8558, #5119 ) ) ;
#6202=CARTESIAN_POINT ( 'NONE',  ( 2.500000000000000000, 2.357898499370433054, -1.951563910473907981E-15 ) ) ;
#6211=CARTESIAN_POINT ( 'NONE',  ( 0.000000000000000000, 1.178949249685218525, 2.041999999999999371 ) ) ;
#6224=CARTESIAN_POINT ( 'NONE',  ( 2.500000000000000000, 1.178949249685213863, -2.042000000000001148 ) ) ;
#6232=FACE_OUTER_BOUND ( 'NONE', #6107, .T. ) ;
#6236=CIRCLE ( 'NONE', #826, 0.2000000000000000944 ) ;
#6238=EDGE_LOOP ( 'NONE', ( #270, #6314, #8233, #2331, #7482 ) ) ;
#6261=VERTEX_POINT ( 'NONE', #3464 ) ;
#6275=CARTESIAN_POINT ( 'NONE',  ( 2.500000000000000000, 0.000000000000000000, 0.000000000000000000 ) ) ;
#6296=ORIENTED_EDGE ( 'NONE', *, *, #2955, .T. ) ;
#6314=ORIENTED_EDGE ( 'NONE', *, *, #5204, .T. ) ;
#6336=CYLINDRICAL_SURFACE ( 'NONE', #5894, 2.500000000000000888 ) ;
#6338=AXIS2_PLACEMENT_3D ( 'NONE', #2940, #6724, #6899 ) ;
#6348=EDGE_CURVE ( 'NONE', #808, #1995, #1726, .T. ) ;
#6349=LINE ( 'NONE', #3093, #4354 ) ;
#6357=FACE_OUTER_BOUND ( 'NONE', #1509, .T. ) ;
#6366=EDGE_CURVE ( 'NONE', #6900, #5850, #2386, .T. ) ;
#6397=AXIS2_PLACEMENT_3D ( 'NONE', #6275, #4978, #267 ) ;
#6414=LINE ( 'NONE', #455, #322 ) ;
#6425=EDGE_LOOP ( 'NONE', ( #7302, #7337, #6948, #341 ) ) ;
#6431=AXIS2_PLACEMENT_3D ( 'NONE', #5271, #5835, #1978 ) ;
#6443=EDGE_CURVE ( 'NONE', #5355, #2563, #1588, .T. ) ;
#6490=ORIENTED_EDGE ( 'NONE', *, *, #1538, .T. ) ;
#6491=DIRECTION ( 'NONE',  ( 0.000000000000000000, -1.287488025362403787E-15, -1.000000000000000000 ) ) ;
#6494=DIRECTION ( 'NONE',  ( -1.000000000000000000, -0.000000000000000000, -0.000000000000000000 ) ) ;
#6499=LINE ( 'NONE', #4501, #5861 ) ;
#6512=PLANE ( 'NONE',  #7030 ) ;
#6513=ORIENTED_EDGE ( 'NONE', *, *, #5601, .T. ) ;
#6539=DIRECTION ( 'NONE',  ( -1.000000000000000000, -0.000000000000000000, -0.000000000000000000 ) ) ;
#6556=FACE_OUTER_BOUND ( 'NONE', #5972, .T. ) ;
#6570=VECTOR ( 'NONE', #2581, 1000.000000000000114 ) ;
#6578=VECTOR ( 'NONE', #7987, 1000.000000000000000 ) ;
#6581=DIRECTION ( 'NONE',  ( 0.000000000000000000, 0.000000000000000000, 1.000000000000000000 ) ) ;
#6591=PRODUCT_DEFINITION ( 'UNKNOWN', '', #4190, #5243 ) ;
#6599=VERTEX_POINT ( 'NONE', #834 ) ;
#6610=EDGE_CURVE ( 'NONE', #2415, #6599, #7626, .T. ) ;
#6621=PRODUCT ( 'socket head cap screw_iso_ISO 4762 M5 x 20 - 20N', 'socket head cap screw_iso_ISO 4762 M5 x 20 - 20N', '', ( #906 ) ) ;
#6640=EDGE_CURVE ( 'NONE', #4446, #3415, #1614, .T. ) ;
#6651=EDGE_CURVE ( 'NONE', #4446, #5850, #5485, .T. ) ;
#6653=ORIENTED_EDGE ( 'NONE', *, *, #934, .T. ) ;
#6661=CARTESIAN_POINT ( 'NONE',  ( 0.000000000000000000, -1.178949249685213863, 2.042000000000002924 ) ) ;
#6667=ORIENTED_EDGE ( 'NONE', *, *, #6099, .T. ) ;
#6696=PLANE ( 'NONE',  #458 ) ;
#6723=ORIENTED_EDGE ( 'NONE', *, *, #5359, .T. ) ;
#6724=DIRECTION ( 'NONE',  ( -1.000000000000000000, -0.000000000000000000, -0.000000000000000000 ) ) ;
#6733=FACE_OUTER_BOUND ( 'NONE', #3841, .T. ) ;
#6755=DIRECTION ( 'NONE',  ( 0.000000000000000000, 0.000000000000000000, 1.000000000000000000 ) ) ;
#6760=ORIENTED_EDGE ( 'NONE', *, *, #6443, .F. ) ;
#6792=DIRECTION ( 'NONE',  ( 0.000000000000000000, 0.8660254037844380415, -0.5000000000000011102 ) ) ;
#6797=DIRECTION ( 'NONE',  ( -0.7071067811865306973, 8.659560562355138702E-17, -0.7071067811865643371 ) ) ;
#6806=DIRECTION ( 'NONE',  ( -1.000000000000000000, -0.000000000000000000, -0.000000000000000000 ) ) ;
#6812=DIRECTION ( 'NONE',  ( 1.000000000000000000, 0.000000000000000000, 0.000000000000000000 ) ) ;
#6816=ORIENTED_EDGE ( 'NONE', *, *, #1488, .F. ) ;
#6832=EDGE_CURVE ( 'NONE', #6599, #5850, #7840, .T. ) ;
#6838=ORIENTED_EDGE ( 'NONE', *, *, #1392, .T. ) ;
#6852=ORIENTED_EDGE ( 'NONE', *, *, #4872, .F. ) ;
#6864=ORIENTED_EDGE ( 'NONE', *, *, #7218, .F. ) ;
#6866=DIRECTION ( 'NONE',  ( -1.000000000000000000, -0.000000000000000000, -0.000000000000000000 ) ) ;
#6878=EDGE_CURVE ( 'NONE', #4350, #1995, #5656, .T. ) ;
#6888=AXIS2_PLACEMENT_3D ( 'NONE', #7181, #1220, #5866 ) ;
#6889=DIRECTION ( 'NONE',  ( -1.000000000000000000, -0.000000000000000000, -0.000000000000000000 ) ) ;
#6899=DIRECTION ( 'NONE',  ( 0.000000000000000000, 0.000000000000000000, 1.000000000000000000 ) ) ;
#6900=VERTEX_POINT ( 'NONE', #1834 ) ;
#6905=LINE ( 'NONE', #1430, #456 ) ;
#6909=EDGE_CURVE ( 'NONE', #1995, #3708, #4507, .T. ) ;
#6924=LINE ( 'NONE', #5491, #7964 ) ;
#6948=ORIENTED_EDGE ( 'NONE', *, *, #7554, .T. ) ;
#6949=PLANE ( 'NONE',  #5493 ) ;
#6961=LINE ( 'NONE', #1617, #8308 ) ;
#6992=FACE_OUTER_BOUND ( 'NONE', #7054, .T. ) ;
#6997=CARTESIAN_POINT ( 'NONE',  ( -31.74999999999995737, 0.000000000000000000, 2.500000000000000888 ) ) ;
#7000=VECTOR ( 'NONE', #1637, 1000.000000000000114 ) ;
#7004=ORIENTED_EDGE ( 'NONE', *, *, #5602, .F. ) ;
#7012=CYLINDRICAL_SURFACE ( 'NONE', #8485, 2.500000000000000888 ) ;
#7017=EDGE_CURVE ( 'NONE', #2221, #848, #4784, .T. ) ;
#7030=AXIS2_PLACEMENT_3D ( 'NONE', #3997, #8048, #1993 ) ;
#7035=ORIENTED_EDGE ( 'NONE', *, *, #3491, .T. ) ;
#7041=DIRECTION ( 'NONE',  ( -1.000000000000000000, -0.000000000000000000, -0.000000000000000000 ) ) ;
#7045=VECTOR ( 'NONE', #8241, 1000.000000000000000 ) ;
#7054=EDGE_LOOP ( 'NONE', ( #6296, #7072 ) ) ;
#7058=DIRECTION ( 'NONE',  ( 1.000000000000000000, 0.000000000000000000, 0.000000000000000000 ) ) ;
#7072=ORIENTED_EDGE ( 'NONE', *, *, #6443, .T. ) ;
#7096=EDGE_CURVE ( 'NONE', #6261, #3580, #4233, .T. ) ;
#7101=DIRECTION ( 'NONE',  ( 0.000000000000000000, 0.000000000000000000, -1.000000000000000000 ) ) ;
#7112=CARTESIAN_POINT ( 'NONE',  ( 2.500000000000000000, 0.000000000000000000, 0.000000000000000000 ) ) ;
#7114=FILL_AREA_STYLE ('',( #4585 ) ) ;
#7125=CIRCLE ( 'NONE', #4900, 2.500000000000000888 ) ;
#7145=CARTESIAN_POINT ( 'NONE',  ( 2.500000000000000000, 1.178949249685213863, -2.042000000000001148 ) ) ;
#7163=DIRECTION ( 'NONE',  ( 0.000000000000000000, 0.000000000000000000, -1.000000000000000000 ) ) ;
#7179=EDGE_CURVE ( 'NONE', #3708, #7568, #199, .T. ) ;
#7180=( GEOMETRIC_REPRESENTATION_CONTEXT ( 3 ) GLOBAL_UNCERTAINTY_ASSIGNED_CONTEXT ( ( #2945 ) ) GLOBAL_UNIT_ASSIGNED_CONTEXT ( ( #2390, #5026, #7817 ) ) REPRESENTATION_CONTEXT ( 'NONE', 'WORKASPACE' ) );
#7181=CARTESIAN_POINT ( 'NONE',  ( 5.000000000000000888, 0.000000000000000000, 0.000000000000000000 ) ) ;
#7182=AXIS2_PLACEMENT_3D ( 'NONE', #4544, #7200, #1239 ) ;
#7184=CARTESIAN_POINT ( 'NONE',  ( 2.500000000000000000, 0.000000000000000000, 0.000000000000000000 ) ) ;
#7193=PLANE ( 'NONE',  #5857 ) ;
#7197=CARTESIAN_POINT ( 'NONE',  ( 2.500000000000000000, -2.357898499370432610, 3.252606517456513302E-15 ) ) ;
#7200=DIRECTION ( 'NONE',  ( -0.000000000000000000, 1.471414886128461471E-15, 1.000000000000000000 ) ) ;
#7209=AXIS2_PLACEMENT_3D ( 'NONE', #7184, #3226, #4740 ) ;
#7218=EDGE_CURVE ( 'NONE', #6599, #1013, #2782, .T. ) ;
#7221=ORIENTED_EDGE ( 'NONE', *, *, #6348, .T. ) ;
#7259=DIRECTION ( 'NONE',  ( -1.000000000000000000, -0.000000000000000000, -0.000000000000000000 ) ) ;
#7261=CIRCLE ( 'NONE', #4906, 4.250000000000000000 ) ;
#7276=DIRECTION ( 'NONE',  ( 1.000000000000000000, 0.000000000000000000, 0.000000000000000000 ) ) ;
#7302=ORIENTED_EDGE ( 'NONE', *, *, #5807, .F. ) ;
#7312=CLOSED_SHELL ( 'NONE', ( #4129, #7895, #597, #4169, #3836, #5760, #5965, #5628, #1859, #5967, #1148, #2692, #6155, #1618, #1491, #501, #3770, #8176, #5100, #629, #8299, #5208, #5139, #4738, #1200, #3673, #4018 ) ) ;
#7319=DIRECTION ( 'NONE',  ( 0.000000000000000000, 0.8660254037844380415, -0.5000000000000012212 ) ) ;
#7337=ORIENTED_EDGE ( 'NONE', *, *, #5602, .T. ) ;
#7338=FACE_OUTER_BOUND ( 'NONE', #1237, .T. ) ;
#7340=ORIENTED_EDGE ( 'NONE', *, *, #7636, .F. ) ;
#7359=CARTESIAN_POINT ( 'NONE',  ( 2.500000000000000000, 2.357898499370433054, -1.951563910473907981E-15 ) ) ;
#7364=AXIS2_PLACEMENT_3D ( 'NONE', #313, #4848, #933 ) ;
#7377=LINE ( 'NONE', #2854, #892 ) ;
#7403=DIRECTION ( 'NONE',  ( 0.000000000000000000, 0.5000000000000012212, 0.8660254037844380415 ) ) ;
#7422=CARTESIAN_POINT ( 'NONE',  ( -31.74999999999995737, 0.000000000000000000, 4.250000000000000000 ) ) ;
#7436=CARTESIAN_POINT ( 'NONE',  ( 2.500000000000000000, 2.357898499370433054, -1.951563910473907981E-15 ) ) ;
#7442=DIRECTION ( 'NONE',  ( 1.000000000000000000, 0.000000000000000000, 0.000000000000000000 ) ) ;
#7449=FACE_OUTER_BOUND ( 'NONE', #3112, .T. ) ;
#7466=FACE_OUTER_BOUND ( 'NONE', #4283, .T. ) ;
#7482=ORIENTED_EDGE ( 'NONE', *, *, #1759, .T. ) ;
#7496=( NAMED_UNIT ( * ) PLANE_ANGLE_UNIT ( ) SI_UNIT ( $, .RADIAN. ) );
#7508=DIRECTION ( 'NONE',  ( 1.000000000000000000, 0.000000000000000000, 0.000000000000000000 ) ) ;
#7516=SHAPE_DEFINITION_REPRESENTATION ( #3225, #1479 ) ;
#7554=EDGE_CURVE ( 'NONE', #5384, #133, #4770, .T. ) ;
#7568=VERTEX_POINT ( 'NONE', #4198 ) ;
#7570=DIRECTION ( 'NONE',  ( 1.000000000000000000, 0.000000000000000000, 0.000000000000000000 ) ) ;
#7578=PLANE ( 'NONE',  #4621 ) ;
#7580=ORIENTED_EDGE ( 'NONE', *, *, #3420, .F. ) ;
#7584=LINE ( 'NONE', #6224, #7045 ) ;
#7619=ORIENTED_EDGE ( 'NONE', *, *, #8016, .F. ) ;
#7626=LINE ( 'NONE', #3490, #6578 ) ;
#7629=ORIENTED_EDGE ( 'NONE', *, *, #2103, .F. ) ;
#7630=PLANE ( 'NONE',  #4023 ) ;
#7636=EDGE_CURVE ( 'NONE', #848, #6900, #6414, .T. ) ;
#7652=ORIENTED_EDGE ( 'NONE', *, *, #6128, .T. ) ;
#7659=CARTESIAN_POINT ( 'NONE',  ( -31.74999999999995737, 0.000000000000000000, 0.000000000000000000 ) ) ;
#7727=DIRECTION ( 'NONE',  ( 0.000000000000000000, 0.000000000000000000, -1.000000000000000000 ) ) ;
#7729=DIRECTION ( 'NONE',  ( -1.000000000000000000, -0.000000000000000000, -0.000000000000000000 ) ) ;
#7738=TOROIDAL_SURFACE ( 'NONE', #6338, 4.000000000000000000, 0.2500000000000000000 ) ;
#7765=DIRECTION ( 'NONE',  ( 0.000000000000000000, 1.000000000000000000, -1.287488025362403787E-15 ) ) ;
#7797=DIRECTION ( 'NONE',  ( -1.000000000000000000, -0.000000000000000000, -0.000000000000000000 ) ) ;
#7817=( NAMED_UNIT ( * ) SI_UNIT ( $, .STERADIAN. ) SOLID_ANGLE_UNIT ( ) );
#7823=EDGE_CURVE ( 'NONE', #1985, #4980, #6499, .T. ) ;
#7840=LINE ( 'NONE', #2496, #8276 ) ;
#7845=ORIENTED_EDGE ( 'NONE', *, *, #3139, .T. ) ;
#7876=DIRECTION ( 'NONE',  ( 0.000000000000000000, 0.000000000000000000, 1.000000000000000000 ) ) ;
#7895=ADVANCED_FACE ( 'NONE', ( #8598 ), #2416, .T. ) ;
#7910=CARTESIAN_POINT ( 'NONE',  ( 25.00000000000000000, 0.000000000000000000, 0.000000000000000000 ) ) ;
#7920=CARTESIAN_POINT ( 'NONE',  ( 2.500000000000000000, 0.000000000000000000, 0.000000000000000000 ) ) ;
#7932=EDGE_CURVE ( 'NONE', #798, #2080, #7125, .T. ) ;
#7934=CARTESIAN_POINT ( 'NONE',  ( 2.500000000000000000, 2.357898499370433054, -1.951563910473907981E-15 ) ) ;
#7944=DIRECTION ( 'NONE',  ( 0.000000000000000000, 0.000000000000000000, 1.000000000000000000 ) ) ;
#7945=ORIENTED_EDGE ( 'NONE', *, *, #121, .F. ) ;
#7964=VECTOR ( 'NONE', #4974, 1000.000000000000114 ) ;
#7973=AXIS2_PLACEMENT_3D ( 'NONE', #2859, #6812, #1422 ) ;
#7974=ORIENTED_EDGE ( 'NONE', *, *, #934, .F. ) ;
#7987=DIRECTION ( 'NONE',  ( -1.000000000000000000, -0.000000000000000000, -0.000000000000000000 ) ) ;
#8003=LINE ( 'NONE', #3339, #5087 ) ;
#8004=ORIENTED_EDGE ( 'NONE', *, *, #5738, .F. ) ;
#8016=EDGE_CURVE ( 'NONE', #2428, #832, #8206, .T. ) ;
#8047=ORIENTED_EDGE ( 'NONE', *, *, #1007, .F. ) ;
#8048=DIRECTION ( 'NONE',  ( 0.000000000000000000, -0.8660254037844390407, -0.4999999999999994449 ) ) ;
#8111=CARTESIAN_POINT ( 'NONE',  ( 0.2500000000000002220, 5.204748896376250699E-16, -4.250000000000000000 ) ) ;
#8154=AXIS2_PLACEMENT_3D ( 'NONE', #7112, #1818, #3725 ) ;
#8157=ORIENTED_EDGE ( 'NONE', *, *, #8016, .T. ) ;
#8176=ADVANCED_FACE ( 'NONE', ( #353 ), #3021, .T. ) ;
#8185=DIRECTION ( 'NONE',  ( 0.000000000000000000, 0.000000000000000000, 1.000000000000000000 ) ) ;
#8193=EDGE_LOOP ( 'NONE', ( #4720, #1072, #5630 ) ) ;
#8201=ORIENTED_EDGE ( 'NONE', *, *, #1731, .T. ) ;
#8206=LINE ( 'NONE', #3411, #4756 ) ;
#8215=VERTEX_POINT ( 'NONE', #8111 ) ;
#8228=ORIENTED_EDGE ( 'NONE', *, *, #5738, .T. ) ;
#8232=CARTESIAN_POINT ( 'NONE',  ( 0.000000000000000000, 0.000000000000000000, 0.000000000000000000 ) ) ;
#8233=ORIENTED_EDGE ( 'NONE', *, *, #121, .T. ) ;
#8241=DIRECTION ( 'NONE',  ( -1.000000000000000000, -0.000000000000000000, -0.000000000000000000 ) ) ;
#8276=VECTOR ( 'NONE', #1796, 1000.000000000000114 ) ;
#8299=ADVANCED_FACE ( 'NONE', ( #1438 ), #7578, .F. ) ;
#8305=DIRECTION ( 'NONE',  ( -1.000000000000000000, -0.000000000000000000, -0.000000000000000000 ) ) ;
#8307=AXIS2_PLACEMENT_3D ( 'NONE', #5153, #6539, #6014 ) ;
#8308=VECTOR ( 'NONE', #5657, 1000.000000000000114 ) ;
#8326=CIRCLE ( 'NONE', #5525, 0.2000000000000000944 ) ;
#8344=EDGE_LOOP ( 'NONE', ( #197, #3276, #6838, #4806 ) ) ;
#8360=LINE ( 'NONE', #6997, #2723 ) ;
#8381=LINE ( 'NONE', #3757, #1395 ) ;
#8402=ORIENTED_EDGE ( 'NONE', *, *, #6128, .F. ) ;
#8434=CIRCLE ( 'NONE', #8154, 2.041999999999999815 ) ;
#8443=ORIENTED_EDGE ( 'NONE', *, *, #7636, .T. ) ;
#8447=MECHANICAL_DESIGN_GEOMETRIC_PRESENTATION_REPRESENTATION('',(#3155),#7180);
#8452=AXIS2_PLACEMENT_3D ( 'NONE', #4528, #5101, #7727 ) ;
#8455=ORIENTED_EDGE ( 'NONE', *, *, #6366, .T. ) ;
#8456=ORIENTED_EDGE ( 'NONE', *, *, #3491, .F. ) ;
#8458=CARTESIAN_POINT ( 'NONE',  ( 2.500000000000000000, 1.178949249685213863, -2.042000000000001148 ) ) ;
#8485=AXIS2_PLACEMENT_3D ( 'NONE', #3016, #671, #6755 ) ;
#8493=DIRECTION ( 'NONE',  ( 1.000000000000000000, 0.000000000000000000, 0.000000000000000000 ) ) ;
#8534=STYLED_ITEM ( 'NONE', ( #2561 ), #1176 ) ;
#8549=EDGE_CURVE ( 'NONE', #832, #2080, #6068, .T. ) ;
#8550=CARTESIAN_POINT ( 'NONE',  ( 2.500000000000000000, -1.178949249685213863, 2.042000000000002924 ) ) ;
#8556=DIRECTION ( 'NONE',  ( 0.000000000000000000, 0.000000000000000000, -1.000000000000000000 ) ) ;
#8558=ORIENTED_EDGE ( 'NONE', *, *, #5331, .T. ) ;
#8577=CIRCLE ( 'NONE', #5358, 2.055000000000000160 ) ;
#8578=DIRECTION ( 'NONE',  ( -1.000000000000000000, -0.000000000000000000, -0.000000000000000000 ) ) ;
#8588=FACE_OUTER_BOUND ( 'NONE', #8193, .T. ) ;
#8598=FACE_OUTER_BOUND ( 'NONE', #1819, .T. ) ;
#8665=COLOUR_RGB('Black',0.12,0.14,0.17);
#8666=FILL_AREA_STYLE_COLOUR('',#8665);
#8667=FILL_AREA_STYLE('',(#8666));
#8668=SURFACE_STYLE_FILL_AREA(#8667);
#8669=SURFACE_SIDE_STYLE('',(#8668));
#8670=SURFACE_STYLE_USAGE(.BOTH.,#8669);
#8671=PRESENTATION_STYLE_ASSIGNMENT((#8670));
ENDSEC;
END-ISO-10303-21;
